ISO-10303-21;
HEADER;
/* Generated by software containing ST-Developer
 * from STEP Tools, Inc. (www.steptools.com) 
 */

FILE_DESCRIPTION(
/* description */ ('Over-Centre Plunger Toggle Clamp on Slotted Fixture Frame'),
/* implementation_level */ '2;1');

FILE_NAME(
/* name */ 
'Flat Washer - M5.step',
/* time_stamp */ '2026-10-28T03:23:24-07:00',
/* author */ (''),
/* organization */ (''),
/* preprocessor_version */ 'ST-DEVELOPER v20.2',
/* originating_system */ 'Autodesk Translation Framework v15.17.0.0',
/* authorisation */ '');

FILE_SCHEMA (('AUTOMOTIVE_DESIGN { 1 0 10303 214 3 1 1 }'));
ENDSEC;

DATA;
#10=MECHANICAL_DESIGN_GEOMETRIC_PRESENTATION_REPRESENTATION('',(#527),#15212);
#405=CONICAL_SURFACE('',#9130,0.275,0.785398163397449);
#443=SHAPE_REPRESENTATION_RELATIONSHIP('SRR','None',#15417,#485);
#485=ADVANCED_BREP_SHAPE_REPRESENTATION('',(#578),#15179);
#527=STYLED_ITEM('',(#15726),#578);
#578=MANIFOLD_SOLID_BREP('Body1',#8259);
#717=FACE_BOUND('',#1892,.T.);
#718=FACE_BOUND('',#1895,.T.);
#925=PLANE('',#9135);
#926=PLANE('',#9139);
#1297=FACE_OUTER_BOUND('',#1889,.T.);
#1298=FACE_OUTER_BOUND('',#1890,.T.);
#1299=FACE_OUTER_BOUND('',#1891,.T.);
#1300=FACE_OUTER_BOUND('',#1893,.T.);
#1301=FACE_OUTER_BOUND('',#1894,.T.);
#1889=EDGE_LOOP('',(#6553,#6554,#6555,#6556));
#1890=EDGE_LOOP('',(#6557,#6558,#6559,#6560));
#1891=EDGE_LOOP('',(#6561));
#1892=EDGE_LOOP('',(#6562));
#1893=EDGE_LOOP('',(#6563,#6564,#6565,#6566));
#1894=EDGE_LOOP('',(#6567));
#1895=EDGE_LOOP('',(#6568));
#2583=LINE('',#13417,#3213);
#2584=LINE('',#13421,#3214);
#2585=LINE('',#13428,#3215);
#3213=VECTOR('',#10844,0.275);
#3214=VECTOR('',#10849,0.265);
#3215=VECTOR('',#10858,0.5);
#3629=CIRCLE('',#9131,0.285);
#3630=CIRCLE('',#9132,0.265);
#3631=CIRCLE('',#9134,0.265);
#3632=CIRCLE('',#9136,0.5);
#3633=CIRCLE('',#9138,0.5);
#4187=VERTEX_POINT('',#13414);
#4188=VERTEX_POINT('',#13416);
#4189=VERTEX_POINT('',#13420);
#4190=VERTEX_POINT('',#13424);
#4191=VERTEX_POINT('',#13427);
#5037=EDGE_CURVE('',#4187,#4187,#3629,.T.);
#5038=EDGE_CURVE('',#4187,#4188,#2583,.T.);
#5039=EDGE_CURVE('',#4188,#4188,#3630,.T.);
#5040=EDGE_CURVE('',#4188,#4189,#2584,.T.);
#5041=EDGE_CURVE('',#4189,#4189,#3631,.T.);
#5042=EDGE_CURVE('',#4190,#4190,#3632,.T.);
#5043=EDGE_CURVE('',#4190,#4191,#2585,.T.);
#5044=EDGE_CURVE('',#4191,#4191,#3633,.T.);
#6553=ORIENTED_EDGE('',*,*,#5037,.T.);
#6554=ORIENTED_EDGE('',*,*,#5038,.T.);
#6555=ORIENTED_EDGE('',*,*,#5039,.T.);
#6556=ORIENTED_EDGE('',*,*,#5038,.F.);
#6557=ORIENTED_EDGE('',*,*,#5039,.F.);
#6558=ORIENTED_EDGE('',*,*,#5040,.T.);
#6559=ORIENTED_EDGE('',*,*,#5041,.T.);
#6560=ORIENTED_EDGE('',*,*,#5040,.F.);
#6561=ORIENTED_EDGE('',*,*,#5042,.T.);
#6562=ORIENTED_EDGE('',*,*,#5037,.F.);
#6563=ORIENTED_EDGE('',*,*,#5042,.F.);
#6564=ORIENTED_EDGE('',*,*,#5043,.T.);
#6565=ORIENTED_EDGE('',*,*,#5044,.T.);
#6566=ORIENTED_EDGE('',*,*,#5043,.F.);
#6567=ORIENTED_EDGE('',*,*,#5044,.F.);
#6568=ORIENTED_EDGE('',*,*,#5041,.F.);
#7685=CYLINDRICAL_SURFACE('',#9133,0.265);
#7686=CYLINDRICAL_SURFACE('',#9137,0.5);
#7969=ADVANCED_FACE('',(#1297),#405,.F.);
#7970=ADVANCED_FACE('',(#1298),#7685,.F.);
#7971=ADVANCED_FACE('',(#1299,#717),#925,.T.);
#7972=ADVANCED_FACE('',(#1300),#7686,.T.);
#7973=ADVANCED_FACE('',(#1301,#718),#926,.F.);
#8259=CLOSED_SHELL('',(#7969,#7970,#7971,#7972,#7973));
#9129=AXIS2_PLACEMENT_3D('',#13412,#10838,#10839);
#9130=AXIS2_PLACEMENT_3D('',#13413,#10840,#10841);
#9131=AXIS2_PLACEMENT_3D('',#13415,#10842,#10843);
#9132=AXIS2_PLACEMENT_3D('',#13418,#10845,#10846);
#9133=AXIS2_PLACEMENT_3D('',#13419,#10847,#10848);
#9134=AXIS2_PLACEMENT_3D('',#13422,#10850,#10851);
#9135=AXIS2_PLACEMENT_3D('',#13423,#10852,#10853);
#9136=AXIS2_PLACEMENT_3D('',#13425,#10854,#10855);
#9137=AXIS2_PLACEMENT_3D('',#13426,#10856,#10857);
#9138=AXIS2_PLACEMENT_3D('',#13429,#10859,#10860);
#9139=AXIS2_PLACEMENT_3D('',#13430,#10861,#10862);
#10838=DIRECTION('axis',(0.,0.,1.));
#10839=DIRECTION('refdir',(1.,0.,0.));
#10840=DIRECTION('center_axis',(0.,1.,0.));
#10841=DIRECTION('ref_axis',(1.,0.,0.));
#10842=DIRECTION('center_axis',(0.,1.,0.));
#10843=DIRECTION('ref_axis',(1.,0.,0.));
#10844=DIRECTION('',(0.707106781186548,-0.707106781186547,-8.65956056235494E-17));
#10845=DIRECTION('center_axis',(0.,-1.,0.));
#10846=DIRECTION('ref_axis',(1.,0.,0.));
#10847=DIRECTION('center_axis',(0.,1.,0.));
#10848=DIRECTION('ref_axis',(1.,0.,0.));
#10849=DIRECTION('',(0.,-1.,0.));
#10850=DIRECTION('center_axis',(0.,-1.,0.));
#10851=DIRECTION('ref_axis',(1.,0.,0.));
#10852=DIRECTION('center_axis',(0.,1.,0.));
#10853=DIRECTION('ref_axis',(1.,0.,0.));
#10854=DIRECTION('center_axis',(0.,1.,0.));
#10855=DIRECTION('ref_axis',(1.,0.,0.));
#10856=DIRECTION('center_axis',(0.,1.,0.));
#10857=DIRECTION('ref_axis',(1.,0.,0.));
#10858=DIRECTION('',(0.,-1.,0.));
#10859=DIRECTION('center_axis',(0.,1.,0.));
#10860=DIRECTION('ref_axis',(1.,0.,0.));
#10861=DIRECTION('center_axis',(0.,1.,0.));
#10862=DIRECTION('ref_axis',(1.,0.,0.));
#13412=CARTESIAN_POINT('',(0.,0.,0.));
#13413=CARTESIAN_POINT('Origin',(0.,0.09,0.));
#13414=CARTESIAN_POINT('',(-0.285,0.1,3.49024337756996E-17));
#13415=CARTESIAN_POINT('Origin',(0.,0.1,0.));
#13416=CARTESIAN_POINT('',(-0.265,0.08,-3.24531401774049E-17));
#13417=CARTESIAN_POINT('',(-0.275,0.09,3.36777869765522E-17));
#13418=CARTESIAN_POINT('Origin',(0.,0.08,0.));
#13419=CARTESIAN_POINT('Origin',(0.,0.,0.));
#13420=CARTESIAN_POINT('',(-0.265,0.,3.24531401774049E-17));
#13421=CARTESIAN_POINT('',(-0.265,0.,3.24531401774049E-17));
#13422=CARTESIAN_POINT('Origin',(0.,0.,0.));
#13423=CARTESIAN_POINT('Origin',(0.,0.1,0.));
#13424=CARTESIAN_POINT('',(-0.5,0.1,6.12323399573677E-17));
#13425=CARTESIAN_POINT('Origin',(0.,0.1,0.));
#13426=CARTESIAN_POINT('Origin',(0.,0.,0.));
#13427=CARTESIAN_POINT('',(-0.5,0.,6.12323399573677E-17));
#13428=CARTESIAN_POINT('',(-0.5,0.,6.12323399573677E-17));
#13429=CARTESIAN_POINT('Origin',(0.,0.,0.));
#13430=CARTESIAN_POINT('Origin',(0.,0.,0.));
#15129=UNCERTAINTY_MEASURE_WITH_UNIT(LENGTH_MEASURE(0.001),#15213,
'DISTANCE_ACCURACY_VALUE',
'Maximum model space distance between geometric entities at asserted c
onnectivities');
#15162=UNCERTAINTY_MEASURE_WITH_UNIT(LENGTH_MEASURE(0.001),#15213,
'DISTANCE_ACCURACY_VALUE',
'Maximum model space distance between geometric entities at asserted c
onnectivities');
#15179=(
GEOMETRIC_REPRESENTATION_CONTEXT(3)
GLOBAL_UNCERTAINTY_ASSIGNED_CONTEXT((#15129))
GLOBAL_UNIT_ASSIGNED_CONTEXT((#15213,#15215,#15216))
REPRESENTATION_CONTEXT('','3D')
);
#15212=(
GEOMETRIC_REPRESENTATION_CONTEXT(3)
GLOBAL_UNCERTAINTY_ASSIGNED_CONTEXT((#15162))
GLOBAL_UNIT_ASSIGNED_CONTEXT((#15213,#15215,#15216))
REPRESENTATION_CONTEXT('','3D')
);
#15213=(
LENGTH_UNIT()
NAMED_UNIT(*)
SI_UNIT(.CENTI.,.METRE.)
);
#15215=(
NAMED_UNIT(*)
PLANE_ANGLE_UNIT()
SI_UNIT($,.RADIAN.)
);
#15216=(
NAMED_UNIT(*)
SI_UNIT($,.STERADIAN.)
SOLID_ANGLE_UNIT()
);
#15233=SHAPE_DEFINITION_REPRESENTATION(#15282,#15417);
#15282=PRODUCT_DEFINITION_SHAPE('',$,#15467);
#15417=SHAPE_REPRESENTATION('',(#9129),#15179);
#15450=PRODUCT_DEFINITION_CONTEXT('part definition',#15599,'design');
#15467=PRODUCT_DEFINITION('Flat Washer - M5','Flat Washer - M5',#15516,
#15450);
#15516=PRODUCT_DEFINITION_FORMATION('',$,#15617);
#15599=APPLICATION_CONTEXT(
'Core Data for Automotive Mechanical Design Process');
#15600=PRODUCT_CONTEXT('part definition',#15599,'mechanical');
#15617=PRODUCT('Flat Washer - M5','Flat Washer - M5','Flat Washer - M5',
(#15600));
#15720=COLOUR_RGB('Black',0.12,0.14,0.17);
#15721=FILL_AREA_STYLE_COLOUR('',#15720);
#15722=FILL_AREA_STYLE('',(#15721));
#15723=SURFACE_STYLE_FILL_AREA(#15722);
#15724=SURFACE_SIDE_STYLE('',(#15723));
#15725=SURFACE_STYLE_USAGE(.BOTH.,#15724);
#15726=PRESENTATION_STYLE_ASSIGNMENT((#15725));
ENDSEC;
END-ISO-10303-21;
